ISO-10303-21;
HEADER;
/* Generated by software containing ST-Developer
 * from STEP Tools, Inc. (www.steptools.com) 
 */

FILE_DESCRIPTION(
/* description */ (''),
/* implementation_level */ '2;1');

FILE_NAME(
/* name */ 'Front_Block.step',
/* time_stamp */ '2026-10-23T22:29:29+06:00',
/* author */ (''),
/* organization */ (''),
/* preprocessor_version */ 'ST-DEVELOPER v20.2',
/* originating_system */ 'Autodesk Translation Framework v15.15.0.0',
/* authorisation */ '');

FILE_SCHEMA (('AUTOMOTIVE_DESIGN { 1 0 10303 214 3 1 1 }'));
ENDSEC;

DATA;
#10=MECHANICAL_DESIGN_GEOMETRIC_PRESENTATION_REPRESENTATION('',(#76),#7047);
#56=SHAPE_REPRESENTATION_RELATIONSHIP('SRR','None',#7089,#66);
#66=ADVANCED_BREP_SHAPE_REPRESENTATION('',(#89),#7041);
#76=STYLED_ITEM('',(#7177),#89);
#89=MANIFOLD_SOLID_BREP('Front_Block',#3401);
#111=FACE_BOUND('',#564,.T.);
#112=FACE_BOUND('',#565,.T.);
#113=FACE_BOUND('',#568,.T.);
#114=FACE_BOUND('',#569,.T.);
#189=PLANE('',#3764);
#190=PLANE('',#3765);
#191=PLANE('',#3766);
#192=PLANE('',#3767);
#193=PLANE('',#3768);
#194=PLANE('',#3771);
#195=PLANE('',#3772);
#196=PLANE('',#3775);
#197=PLANE('',#3776);
#198=PLANE('',#3779);
#366=FACE_OUTER_BOUND('',#559,.T.);
#367=FACE_OUTER_BOUND('',#560,.T.);
#368=FACE_OUTER_BOUND('',#561,.T.);
#369=FACE_OUTER_BOUND('',#562,.T.);
#370=FACE_OUTER_BOUND('',#563,.T.);
#371=FACE_OUTER_BOUND('',#566,.T.);
#372=FACE_OUTER_BOUND('',#567,.T.);
#373=FACE_OUTER_BOUND('',#570,.T.);
#374=FACE_OUTER_BOUND('',#571,.T.);
#375=FACE_OUTER_BOUND('',#572,.T.);
#376=FACE_OUTER_BOUND('',#573,.T.);
#377=FACE_OUTER_BOUND('',#574,.T.);
#559=EDGE_LOOP('',(#2725,#2726,#2727,#2728));
#560=EDGE_LOOP('',(#2729,#2730,#2731,#2732));
#561=EDGE_LOOP('',(#2733,#2734,#2735,#2736));
#562=EDGE_LOOP('',(#2737,#2738,#2739,#2740));
#563=EDGE_LOOP('',(#2741,#2742,#2743,#2744,#2745,#2746,#2747,#2748));
#564=EDGE_LOOP('',(#2749));
#565=EDGE_LOOP('',(#2750));
#566=EDGE_LOOP('',(#2751,#2752,#2753,#2754,#2755,#2756,#2757,#2758));
#567=EDGE_LOOP('',(#2759,#2760,#2761,#2762));
#568=EDGE_LOOP('',(#2763));
#569=EDGE_LOOP('',(#2764));
#570=EDGE_LOOP('',(#2765,#2766,#2767,#2768));
#571=EDGE_LOOP('',(#2769,#2770,#2771,#2772));
#572=EDGE_LOOP('',(#2773,#2774,#2775,#2776));
#573=EDGE_LOOP('',(#2777,#2778,#2779,#2780));
#574=EDGE_LOOP('',(#2781,#2782,#2783,#2784));
#770=CIRCLE('',#3769,2.5175);
#771=CIRCLE('',#3770,2.5175);
#772=CIRCLE('',#3773,2.5175);
#773=CIRCLE('',#3774,2.5175);
#923=LINE('',#5683,#1217);
#924=LINE('',#5685,#1218);
#925=LINE('',#5687,#1219);
#926=LINE('',#5688,#1220);
#927=LINE('',#5691,#1221);
#928=LINE('',#5693,#1222);
#929=LINE('',#5694,#1223);
#930=LINE('',#5697,#1224);
#931=LINE('',#5699,#1225);
#932=LINE('',#5700,#1226);
#933=LINE('',#5702,#1227);
#934=LINE('',#5705,#1228);
#935=LINE('',#5707,#1229);
#936=LINE('',#5709,#1230);
#937=LINE('',#5711,#1231);
#938=LINE('',#5712,#1232);
#939=LINE('',#5719,#1233);
#940=LINE('',#5721,#1234);
#941=LINE('',#5722,#1235);
#942=LINE('',#5725,#1236);
#943=LINE('',#5727,#1237);
#944=LINE('',#5728,#1238);
#945=LINE('',#5734,#1239);
#946=LINE('',#5736,#1240);
#947=LINE('',#5738,#1241);
#948=LINE('',#5740,#1242);
#1217=VECTOR('',#4482,10.);
#1218=VECTOR('',#4483,10.);
#1219=VECTOR('',#4484,10.);
#1220=VECTOR('',#4485,10.);
#1221=VECTOR('',#4488,10.);
#1222=VECTOR('',#4489,10.);
#1223=VECTOR('',#4490,10.);
#1224=VECTOR('',#4493,10.);
#1225=VECTOR('',#4494,10.);
#1226=VECTOR('',#4495,10.);
#1227=VECTOR('',#4498,10.);
#1228=VECTOR('',#4501,10.);
#1229=VECTOR('',#4502,10.);
#1230=VECTOR('',#4503,10.);
#1231=VECTOR('',#4504,10.);
#1232=VECTOR('',#4505,10.);
#1233=VECTOR('',#4512,10.);
#1234=VECTOR('',#4513,10.);
#1235=VECTOR('',#4514,10.);
#1236=VECTOR('',#4517,10.);
#1237=VECTOR('',#4518,10.);
#1238=VECTOR('',#4519,10.);
#1239=VECTOR('',#4526,10.);
#1240=VECTOR('',#4529,10.);
#1241=VECTOR('',#4532,3.25);
#1242=VECTOR('',#4535,3.25);
#1596=VERTEX_POINT('',#5681);
#1597=VERTEX_POINT('',#5682);
#1598=VERTEX_POINT('',#5684);
#1599=VERTEX_POINT('',#5686);
#1600=VERTEX_POINT('',#5690);
#1601=VERTEX_POINT('',#5692);
#1602=VERTEX_POINT('',#5696);
#1603=VERTEX_POINT('',#5698);
#1604=VERTEX_POINT('',#5704);
#1605=VERTEX_POINT('',#5706);
#1606=VERTEX_POINT('',#5708);
#1607=VERTEX_POINT('',#5710);
#1608=VERTEX_POINT('',#5713);
#1609=VERTEX_POINT('',#5715);
#1610=VERTEX_POINT('',#5718);
#1611=VERTEX_POINT('',#5720);
#1612=VERTEX_POINT('',#5724);
#1613=VERTEX_POINT('',#5726);
#1614=VERTEX_POINT('',#5729);
#1615=VERTEX_POINT('',#5731);
#1997=EDGE_CURVE('',#1596,#1597,#923,.T.);
#1998=EDGE_CURVE('',#1598,#1596,#924,.T.);
#1999=EDGE_CURVE('',#1599,#1598,#925,.T.);
#2000=EDGE_CURVE('',#1597,#1599,#926,.T.);
#2001=EDGE_CURVE('',#1597,#1600,#927,.T.);
#2002=EDGE_CURVE('',#1601,#1599,#928,.T.);
#2003=EDGE_CURVE('',#1600,#1601,#929,.T.);
#2004=EDGE_CURVE('',#1600,#1602,#930,.T.);
#2005=EDGE_CURVE('',#1603,#1601,#931,.T.);
#2006=EDGE_CURVE('',#1602,#1603,#932,.T.);
#2007=EDGE_CURVE('',#1603,#1598,#933,.T.);
#2008=EDGE_CURVE('',#1596,#1604,#934,.T.);
#2009=EDGE_CURVE('',#1604,#1605,#935,.T.);
#2010=EDGE_CURVE('',#1605,#1606,#936,.T.);
#2011=EDGE_CURVE('',#1606,#1607,#937,.T.);
#2012=EDGE_CURVE('',#1607,#1602,#938,.T.);
#2013=EDGE_CURVE('',#1608,#1608,#770,.F.);
#2014=EDGE_CURVE('',#1609,#1609,#771,.F.);
#2015=EDGE_CURVE('',#1610,#1607,#939,.T.);
#2016=EDGE_CURVE('',#1611,#1610,#940,.T.);
#2017=EDGE_CURVE('',#1604,#1611,#941,.T.);
#2018=EDGE_CURVE('',#1610,#1612,#942,.T.);
#2019=EDGE_CURVE('',#1612,#1613,#943,.T.);
#2020=EDGE_CURVE('',#1613,#1611,#944,.T.);
#2021=EDGE_CURVE('',#1614,#1614,#772,.T.);
#2022=EDGE_CURVE('',#1615,#1615,#773,.T.);
#2023=EDGE_CURVE('',#1606,#1612,#945,.T.);
#2024=EDGE_CURVE('',#1605,#1613,#946,.T.);
#2025=EDGE_CURVE('',#1615,#1608,#947,.T.);
#2026=EDGE_CURVE('',#1614,#1609,#948,.T.);
#2725=ORIENTED_EDGE('',*,*,#1997,.F.);
#2726=ORIENTED_EDGE('',*,*,#1998,.F.);
#2727=ORIENTED_EDGE('',*,*,#1999,.F.);
#2728=ORIENTED_EDGE('',*,*,#2000,.F.);
#2729=ORIENTED_EDGE('',*,*,#2001,.F.);
#2730=ORIENTED_EDGE('',*,*,#2000,.T.);
#2731=ORIENTED_EDGE('',*,*,#2002,.F.);
#2732=ORIENTED_EDGE('',*,*,#2003,.F.);
#2733=ORIENTED_EDGE('',*,*,#2004,.F.);
#2734=ORIENTED_EDGE('',*,*,#2003,.T.);
#2735=ORIENTED_EDGE('',*,*,#2005,.F.);
#2736=ORIENTED_EDGE('',*,*,#2006,.F.);
#2737=ORIENTED_EDGE('',*,*,#2007,.F.);
#2738=ORIENTED_EDGE('',*,*,#2005,.T.);
#2739=ORIENTED_EDGE('',*,*,#2002,.T.);
#2740=ORIENTED_EDGE('',*,*,#1999,.T.);
#2741=ORIENTED_EDGE('',*,*,#2006,.T.);
#2742=ORIENTED_EDGE('',*,*,#2007,.T.);
#2743=ORIENTED_EDGE('',*,*,#1998,.T.);
#2744=ORIENTED_EDGE('',*,*,#2008,.T.);
#2745=ORIENTED_EDGE('',*,*,#2009,.T.);
#2746=ORIENTED_EDGE('',*,*,#2010,.T.);
#2747=ORIENTED_EDGE('',*,*,#2011,.T.);
#2748=ORIENTED_EDGE('',*,*,#2012,.T.);
#2749=ORIENTED_EDGE('',*,*,#2013,.T.);
#2750=ORIENTED_EDGE('',*,*,#2014,.T.);
#2751=ORIENTED_EDGE('',*,*,#2004,.T.);
#2752=ORIENTED_EDGE('',*,*,#2012,.F.);
#2753=ORIENTED_EDGE('',*,*,#2015,.F.);
#2754=ORIENTED_EDGE('',*,*,#2016,.F.);
#2755=ORIENTED_EDGE('',*,*,#2017,.F.);
#2756=ORIENTED_EDGE('',*,*,#2008,.F.);
#2757=ORIENTED_EDGE('',*,*,#1997,.T.);
#2758=ORIENTED_EDGE('',*,*,#2001,.T.);
#2759=ORIENTED_EDGE('',*,*,#2016,.T.);
#2760=ORIENTED_EDGE('',*,*,#2018,.T.);
#2761=ORIENTED_EDGE('',*,*,#2019,.T.);
#2762=ORIENTED_EDGE('',*,*,#2020,.T.);
#2763=ORIENTED_EDGE('',*,*,#2021,.T.);
#2764=ORIENTED_EDGE('',*,*,#2022,.T.);
#2765=ORIENTED_EDGE('',*,*,#2015,.T.);
#2766=ORIENTED_EDGE('',*,*,#2011,.F.);
#2767=ORIENTED_EDGE('',*,*,#2023,.T.);
#2768=ORIENTED_EDGE('',*,*,#2018,.F.);
#2769=ORIENTED_EDGE('',*,*,#2017,.T.);
#2770=ORIENTED_EDGE('',*,*,#2020,.F.);
#2771=ORIENTED_EDGE('',*,*,#2024,.F.);
#2772=ORIENTED_EDGE('',*,*,#2009,.F.);
#2773=ORIENTED_EDGE('',*,*,#2022,.F.);
#2774=ORIENTED_EDGE('',*,*,#2025,.T.);
#2775=ORIENTED_EDGE('',*,*,#2013,.F.);
#2776=ORIENTED_EDGE('',*,*,#2025,.F.);
#2777=ORIENTED_EDGE('',*,*,#2021,.F.);
#2778=ORIENTED_EDGE('',*,*,#2026,.T.);
#2779=ORIENTED_EDGE('',*,*,#2014,.F.);
#2780=ORIENTED_EDGE('',*,*,#2026,.F.);
#2781=ORIENTED_EDGE('',*,*,#2010,.F.);
#2782=ORIENTED_EDGE('',*,*,#2024,.T.);
#2783=ORIENTED_EDGE('',*,*,#2019,.F.);
#2784=ORIENTED_EDGE('',*,*,#2023,.F.);
#3197=CYLINDRICAL_SURFACE('',#3777,2.5175);
#3198=CYLINDRICAL_SURFACE('',#3778,2.5175);
#3308=ADVANCED_FACE('',(#366),#189,.T.);
#3309=ADVANCED_FACE('',(#367),#190,.T.);
#3310=ADVANCED_FACE('',(#368),#191,.T.);
#3311=ADVANCED_FACE('',(#369),#192,.T.);
#3312=ADVANCED_FACE('',(#370,#111,#112),#193,.F.);
#3313=ADVANCED_FACE('',(#371),#194,.F.);
#3314=ADVANCED_FACE('',(#372,#113,#114),#195,.T.);
#3315=ADVANCED_FACE('',(#373),#196,.T.);
#3316=ADVANCED_FACE('',(#374),#197,.T.);
#3317=ADVANCED_FACE('',(#375),#3197,.F.);
#3318=ADVANCED_FACE('',(#376),#3198,.F.);
#3319=ADVANCED_FACE('',(#377),#198,.T.);
#3401=CLOSED_SHELL('',(#3308,#3309,#3310,#3311,#3312,#3313,#3314,#3315,
#3316,#3317,#3318,#3319));
#3763=AXIS2_PLACEMENT_3D('',#5679,#4478,#4479);
#3764=AXIS2_PLACEMENT_3D('',#5680,#4480,#4481);
#3765=AXIS2_PLACEMENT_3D('',#5689,#4486,#4487);
#3766=AXIS2_PLACEMENT_3D('',#5695,#4491,#4492);
#3767=AXIS2_PLACEMENT_3D('',#5701,#4496,#4497);
#3768=AXIS2_PLACEMENT_3D('',#5703,#4499,#4500);
#3769=AXIS2_PLACEMENT_3D('',#5714,#4506,#4507);
#3770=AXIS2_PLACEMENT_3D('',#5716,#4508,#4509);
#3771=AXIS2_PLACEMENT_3D('',#5717,#4510,#4511);
#3772=AXIS2_PLACEMENT_3D('',#5723,#4515,#4516);
#3773=AXIS2_PLACEMENT_3D('',#5730,#4520,#4521);
#3774=AXIS2_PLACEMENT_3D('',#5732,#4522,#4523);
#3775=AXIS2_PLACEMENT_3D('',#5733,#4524,#4525);
#3776=AXIS2_PLACEMENT_3D('',#5735,#4527,#4528);
#3777=AXIS2_PLACEMENT_3D('',#5737,#4530,#4531);
#3778=AXIS2_PLACEMENT_3D('',#5739,#4533,#4534);
#3779=AXIS2_PLACEMENT_3D('',#5741,#4536,#4537);
#4478=DIRECTION('axis',(0.,0.,1.));
#4479=DIRECTION('refdir',(1.,0.,0.));
#4480=DIRECTION('center_axis',(0.,-1.,0.));
#4481=DIRECTION('ref_axis',(0.,0.,-1.));
#4482=DIRECTION('',(0.,0.,1.));
#4483=DIRECTION('',(-1.,0.,0.));
#4484=DIRECTION('',(0.,0.,-1.));
#4485=DIRECTION('',(1.,0.,0.));
#4486=DIRECTION('center_axis',(0.,0.,-1.));
#4487=DIRECTION('ref_axis',(0.,1.,0.));
#4488=DIRECTION('',(0.,-1.,0.));
#4489=DIRECTION('',(0.,1.,0.));
#4490=DIRECTION('',(1.,0.,0.));
#4491=DIRECTION('center_axis',(0.,1.,0.));
#4492=DIRECTION('ref_axis',(0.,0.,1.));
#4493=DIRECTION('',(0.,0.,-1.));
#4494=DIRECTION('',(0.,0.,1.));
#4495=DIRECTION('',(1.,0.,0.));
#4496=DIRECTION('center_axis',(-1.,0.,0.));
#4497=DIRECTION('ref_axis',(0.,0.,1.));
#4498=DIRECTION('',(0.,1.,0.));
#4499=DIRECTION('center_axis',(0.,0.,1.));
#4500=DIRECTION('ref_axis',(1.,0.,0.));
#4501=DIRECTION('',(0.,1.,0.));
#4502=DIRECTION('',(1.,0.,0.));
#4503=DIRECTION('',(0.,-1.,0.));
#4504=DIRECTION('',(-1.,0.,0.));
#4505=DIRECTION('',(0.,1.,0.));
#4506=DIRECTION('center_axis',(0.,0.,-1.));
#4507=DIRECTION('ref_axis',(-1.,0.,0.));
#4508=DIRECTION('center_axis',(0.,0.,-1.));
#4509=DIRECTION('ref_axis',(-1.,0.,0.));
#4510=DIRECTION('center_axis',(1.,0.,0.));
#4511=DIRECTION('ref_axis',(0.,-1.,0.));
#4512=DIRECTION('',(0.,0.,-1.));
#4513=DIRECTION('',(0.,-1.,0.));
#4514=DIRECTION('',(0.,0.,1.));
#4515=DIRECTION('center_axis',(0.,0.,1.));
#4516=DIRECTION('ref_axis',(1.,0.,0.));
#4517=DIRECTION('',(1.,0.,0.));
#4518=DIRECTION('',(0.,1.,0.));
#4519=DIRECTION('',(-1.,0.,0.));
#4520=DIRECTION('center_axis',(0.,0.,-1.));
#4521=DIRECTION('ref_axis',(-1.,0.,0.));
#4522=DIRECTION('center_axis',(0.,0.,-1.));
#4523=DIRECTION('ref_axis',(-1.,0.,0.));
#4524=DIRECTION('center_axis',(0.,-1.,0.));
#4525=DIRECTION('ref_axis',(1.,0.,0.));
#4526=DIRECTION('',(0.,0.,1.));
#4527=DIRECTION('center_axis',(0.,1.,0.));
#4528=DIRECTION('ref_axis',(-1.,0.,0.));
#4529=DIRECTION('',(0.,0.,1.));
#4530=DIRECTION('center_axis',(0.,0.,1.));
#4531=DIRECTION('ref_axis',(-1.,0.,0.));
#4532=DIRECTION('',(0.,0.,-1.));
#4533=DIRECTION('center_axis',(0.,0.,-1.));
#4534=DIRECTION('ref_axis',(-1.,0.,0.));
#4535=DIRECTION('',(0.,0.,-1.));
#4536=DIRECTION('center_axis',(1.,0.,0.));
#4537=DIRECTION('ref_axis',(0.,1.,0.));
#5679=CARTESIAN_POINT('',(0.,0.,0.));
#5680=CARTESIAN_POINT('Origin',(29.1374542444053,4.,6.));
#5681=CARTESIAN_POINT('',(29.6374542444053,4.,0.));
#5682=CARTESIAN_POINT('',(29.6374542444053,4.,6.));
#5683=CARTESIAN_POINT('',(29.6374542444053,4.,11.));
#5684=CARTESIAN_POINT('',(35.1374542444053,4.,0.));
#5685=CARTESIAN_POINT('',(14.5687271222026,4.,0.));
#5686=CARTESIAN_POINT('',(35.1374542444053,4.,6.));
#5687=CARTESIAN_POINT('',(35.1374542444053,4.,6.));
#5688=CARTESIAN_POINT('',(29.1374542444053,4.,6.));
#5689=CARTESIAN_POINT('Origin',(29.1374542444053,-4.,6.));
#5690=CARTESIAN_POINT('',(29.6374542444053,-4.,6.));
#5691=CARTESIAN_POINT('',(29.6374542444053,13.,6.));
#5692=CARTESIAN_POINT('',(35.1374542444053,-4.,6.));
#5693=CARTESIAN_POINT('',(35.1374542444053,-4.,6.));
#5694=CARTESIAN_POINT('',(29.1374542444053,-4.,6.));
#5695=CARTESIAN_POINT('Origin',(29.1374542444053,-4.,0.));
#5696=CARTESIAN_POINT('',(29.6374542444053,-4.,0.));
#5697=CARTESIAN_POINT('',(29.6374542444053,-4.,8.));
#5698=CARTESIAN_POINT('',(35.1374542444053,-4.,0.));
#5699=CARTESIAN_POINT('',(35.1374542444053,-4.,-6.));
#5700=CARTESIAN_POINT('',(14.5687271222026,-4.,0.));
#5701=CARTESIAN_POINT('Origin',(35.1374542444053,0.,3.));
#5702=CARTESIAN_POINT('',(35.1374542444053,0.,0.));
#5703=CARTESIAN_POINT('Origin',(0.,0.,0.));
#5704=CARTESIAN_POINT('',(29.6374542444053,30.,0.));
#5705=CARTESIAN_POINT('',(29.6374542444053,15.,0.));
#5706=CARTESIAN_POINT('',(50.,30.,0.));
#5707=CARTESIAN_POINT('',(-50.,30.,0.));
#5708=CARTESIAN_POINT('',(50.,-30.,0.));
#5709=CARTESIAN_POINT('',(50.,30.,0.));
#5710=CARTESIAN_POINT('',(29.6374542444053,-30.,0.));
#5711=CARTESIAN_POINT('',(50.,-30.,0.));
#5712=CARTESIAN_POINT('',(29.6374542444053,15.,0.));
#5713=CARTESIAN_POINT('',(44.5175,22.,0.));
#5714=CARTESIAN_POINT('Origin',(42.,22.,0.));
#5715=CARTESIAN_POINT('',(44.5175,-22.,0.));
#5716=CARTESIAN_POINT('Origin',(42.,-22.,0.));
#5717=CARTESIAN_POINT('Origin',(29.6374542444053,30.,16.));
#5718=CARTESIAN_POINT('',(29.6374542444053,-30.,16.));
#5719=CARTESIAN_POINT('',(29.6374542444053,-30.,8.));
#5720=CARTESIAN_POINT('',(29.6374542444053,30.,16.));
#5721=CARTESIAN_POINT('',(29.6374542444053,15.,16.));
#5722=CARTESIAN_POINT('',(29.6374542444053,30.,8.));
#5723=CARTESIAN_POINT('Origin',(0.,0.,16.));
#5724=CARTESIAN_POINT('',(50.,-30.,16.));
#5725=CARTESIAN_POINT('',(50.,-30.,16.));
#5726=CARTESIAN_POINT('',(50.,30.,16.));
#5727=CARTESIAN_POINT('',(50.,30.,16.));
#5728=CARTESIAN_POINT('',(-50.,30.,16.));
#5729=CARTESIAN_POINT('',(44.5175,-22.,16.));
#5730=CARTESIAN_POINT('Origin',(42.,-22.,16.));
#5731=CARTESIAN_POINT('',(44.5175,22.,16.));
#5732=CARTESIAN_POINT('Origin',(42.,22.,16.));
#5733=CARTESIAN_POINT('Origin',(-50.,-30.,0.));
#5734=CARTESIAN_POINT('',(50.,-30.,0.));
#5735=CARTESIAN_POINT('Origin',(50.,30.,0.));
#5736=CARTESIAN_POINT('',(50.,30.,0.));
#5737=CARTESIAN_POINT('Origin',(42.,22.,16.));
#5738=CARTESIAN_POINT('',(44.5175,22.,16.));
#5739=CARTESIAN_POINT('Origin',(42.,-22.,16.));
#5740=CARTESIAN_POINT('',(44.5175,-22.,16.));
#5741=CARTESIAN_POINT('Origin',(50.,-30.,0.));
#7029=UNCERTAINTY_MEASURE_WITH_UNIT(LENGTH_MEASURE(0.01),#7048,
'DISTANCE_ACCURACY_VALUE',
'Maximum model space distance between geometric entities at asserted c
onnectivities');
#7035=UNCERTAINTY_MEASURE_WITH_UNIT(LENGTH_MEASURE(0.01),#7048,
'DISTANCE_ACCURACY_VALUE',
'Maximum model space distance between geometric entities at asserted c
onnectivities');
#7041=(
GEOMETRIC_REPRESENTATION_CONTEXT(3)
GLOBAL_UNCERTAINTY_ASSIGNED_CONTEXT((#7029))
GLOBAL_UNIT_ASSIGNED_CONTEXT((#7048,#7050,#7051))
REPRESENTATION_CONTEXT('','3D')
);
#7047=(
GEOMETRIC_REPRESENTATION_CONTEXT(3)
GLOBAL_UNCERTAINTY_ASSIGNED_CONTEXT((#7035))
GLOBAL_UNIT_ASSIGNED_CONTEXT((#7048,#7050,#7051))
REPRESENTATION_CONTEXT('','3D')
);
#7048=(
LENGTH_UNIT()
NAMED_UNIT(*)
SI_UNIT(.MILLI.,.METRE.)
);
#7050=(
NAMED_UNIT(*)
PLANE_ANGLE_UNIT()
SI_UNIT($,.RADIAN.)
);
#7051=(
NAMED_UNIT(*)
SI_UNIT($,.STERADIAN.)
SOLID_ANGLE_UNIT()
);
#7057=SHAPE_DEFINITION_REPRESENTATION(#7068,#7089);
#7068=PRODUCT_DEFINITION_SHAPE('',$,#7101);
#7089=SHAPE_REPRESENTATION('',(#3763),#7041);
#7095=PRODUCT_DEFINITION_CONTEXT('part definition',#7130,'design');
#7101=PRODUCT_DEFINITION('Front_Block','Front_Block',#7112,#7095);
#7112=PRODUCT_DEFINITION_FORMATION('',$,#7137);
#7130=APPLICATION_CONTEXT(
'Core Data for Automotive Mechanical Design Process');
#7131=PRODUCT_CONTEXT('part definition',#7130,'mechanical');
#7137=PRODUCT('Front_Block','Front_Block',$,(#7131));
#7171=COLOUR_RGB('Dark Blue',0.08,0.2,0.34);
#7172=FILL_AREA_STYLE_COLOUR('',#7171);
#7173=FILL_AREA_STYLE('',(#7172));
#7174=SURFACE_STYLE_FILL_AREA(#7173);
#7175=SURFACE_SIDE_STYLE('',(#7174));
#7176=SURFACE_STYLE_USAGE(.BOTH.,#7175);
#7177=PRESENTATION_STYLE_ASSIGNMENT((#7176));
ENDSEC;
END-ISO-10303-21;
